ISO-10303-21;
HEADER;
/* Generated by software containing ST-Developer
 * from STEP Tools, Inc. (www.steptools.com) 
 */

FILE_DESCRIPTION(
/* description */ (''),
/* implementation_level */ '2;1');

FILE_NAME(
/* name */ 'Ball_03.step',
/* time_stamp */ '2026-10-04T23:23:09-07:00',
/* author */ (''),
/* organization */ (''),
/* preprocessor_version */ 'ST-DEVELOPER v20.2',
/* originating_system */ 'Autodesk Translation Framework v15.15.0.0',
/* authorisation */ '');

FILE_SCHEMA (('AUTOMOTIVE_DESIGN { 1 0 10303 214 3 1 1 }'));
ENDSEC;

DATA;
#10=MECHANICAL_DESIGN_GEOMETRIC_PRESENTATION_REPRESENTATION('',(#74),#2676);
#48=SPHERICAL_SURFACE('',#1712,1.);
#55=SHAPE_REPRESENTATION_RELATIONSHIP('SRR','None',#2714,#63);
#63=ADVANCED_BREP_SHAPE_REPRESENTATION('',(#85),#2674);
#74=STYLED_ITEM('',(#2757),#85);
#85=MANIFOLD_SOLID_BREP('Body1',#1485);
#254=FACE_OUTER_BOUND('',#372,.T.);
#372=EDGE_LOOP('',(#1218,#1219));
#690=CIRCLE('',#1713,1.);
#773=VERTEX_POINT('',#2503);
#774=VERTEX_POINT('',#2504);
#927=EDGE_CURVE('',#773,#774,#690,.T.);
#1218=ORIENTED_EDGE('',*,*,#927,.T.);
#1219=ORIENTED_EDGE('',*,*,#927,.F.);
#1445=ADVANCED_FACE('',(#254),#48,.T.);
#1485=CLOSED_SHELL('',(#1445));
#1711=AXIS2_PLACEMENT_3D('',#2501,#2081,#2082);
#1712=AXIS2_PLACEMENT_3D('',#2502,#2083,#2084);
#1713=AXIS2_PLACEMENT_3D('',#2505,#2085,#2086);
#2081=DIRECTION('axis',(0.,0.,1.));
#2082=DIRECTION('refdir',(1.,0.,0.));
#2083=DIRECTION('center_axis',(0.,0.,1.));
#2084=DIRECTION('ref_axis',(-1.,0.,0.));
#2085=DIRECTION('center_axis',(0.,1.,0.));
#2086=DIRECTION('ref_axis',(1.,0.,0.));
#2501=CARTESIAN_POINT('',(0.,0.,0.));
#2502=CARTESIAN_POINT('Origin',(-8.,-7.5,4.));
#2503=CARTESIAN_POINT('',(-8.,-7.5,5.));
#2504=CARTESIAN_POINT('',(-8.,-7.5,3.));
#2505=CARTESIAN_POINT('Origin',(-8.,-7.5,4.));
#2664=UNCERTAINTY_MEASURE_WITH_UNIT(LENGTH_MEASURE(0.01),#2677,
'DISTANCE_ACCURACY_VALUE',
'Maximum model space distance between geometric entities at asserted c
onnectivities');
#2666=UNCERTAINTY_MEASURE_WITH_UNIT(LENGTH_MEASURE(0.01),#2677,
'DISTANCE_ACCURACY_VALUE',
'Maximum model space distance between geometric entities at asserted c
onnectivities');
#2674=(
GEOMETRIC_REPRESENTATION_CONTEXT(3)
GLOBAL_UNCERTAINTY_ASSIGNED_CONTEXT((#2664))
GLOBAL_UNIT_ASSIGNED_CONTEXT((#2677,#2679,#2680))
REPRESENTATION_CONTEXT('','3D')
);
#2676=(
GEOMETRIC_REPRESENTATION_CONTEXT(3)
GLOBAL_UNCERTAINTY_ASSIGNED_CONTEXT((#2666))
GLOBAL_UNIT_ASSIGNED_CONTEXT((#2677,#2679,#2680))
REPRESENTATION_CONTEXT('','3D')
);
#2677=(
LENGTH_UNIT()
NAMED_UNIT(*)
SI_UNIT(.MILLI.,.METRE.)
);
#2679=(
NAMED_UNIT(*)
PLANE_ANGLE_UNIT()
SI_UNIT($,.RADIAN.)
);
#2680=(
NAMED_UNIT(*)
SI_UNIT($,.STERADIAN.)
SOLID_ANGLE_UNIT()
);
#2688=SHAPE_DEFINITION_REPRESENTATION(#2697,#2714);
#2697=PRODUCT_DEFINITION_SHAPE('',$,#2724);
#2714=SHAPE_REPRESENTATION('',(#1711),#2674);
#2716=PRODUCT_DEFINITION_CONTEXT('part definition',#2745,'design');
#2724=PRODUCT_DEFINITION('Ball_03','Ball_03',#2733,#2716);
#2733=PRODUCT_DEFINITION_FORMATION('',$,#2754);
#2745=APPLICATION_CONTEXT(
'Core Data for Automotive Mechanical Design Process');
#2746=PRODUCT_CONTEXT('part definition',#2745,'mechanical');
#2754=PRODUCT('Ball_03','Ball_03',$,(#2746));
#2757=PRESENTATION_STYLE_ASSIGNMENT((#2759));
#2759=SURFACE_STYLE_USAGE(.BOTH.,#2761);
#2761=SURFACE_SIDE_STYLE('',(#2763));
#2763=SURFACE_STYLE_FILL_AREA(#2765);
#2765=FILL_AREA_STYLE('Opaque(203,203,203)',(#2767));
#2767=FILL_AREA_STYLE_COLOUR('Opaque(203,203,203)',#2769);
#2769=COLOUR_RGB('Opaque(203,203,203)', 0.09019608, 0.27058824, 0.51372549);
ENDSEC;
END-ISO-10303-21;
